ISO-10303-21;
HEADER;
/* Generated by software containing ST-Developer
 * from STEP Tools, Inc. (www.steptools.com) 
 */

FILE_DESCRIPTION(
/* description */ ('Line shaft on three pillow blocks'),
/* implementation_level */ '2;1');

FILE_NAME(
/* name */ 'Cap Screw - M6x25.step',
/* time_stamp */ '2026-10-27T10:49:19-07:00',
/* author */ (''),
/* organization */ (''),
/* preprocessor_version */ 'ST-DEVELOPER v20.2',
/* originating_system */ 'Autodesk Translation Framework v15.17.0.0',
/* authorisation */ '');

FILE_SCHEMA (('AUTOMOTIVE_DESIGN { 1 0 10303 214 3 1 1 }'));
ENDSEC;

DATA;
#10=MECHANICAL_DESIGN_GEOMETRIC_PRESENTATION_REPRESENTATION('',(#350),#8377);
#265=ORIENTED_CLOSED_SHELL('',*,#4337,.F.);
#268=CONICAL_SURFACE('',#4802,0.475,0.785398163397449);
#269=CONICAL_SURFACE('',#4806,0.485,0.785398163397448);
#270=CONICAL_SURFACE('',#4810,0.31,0.463647609000806);
#271=CONICAL_SURFACE('',#4814,0.27,0.785398163397448);
#281=BREP_WITH_VOIDS('Body1',#4336,(#265));
#296=SHAPE_REPRESENTATION_RELATIONSHIP('SRR','None',#8511,#323);
#323=ADVANCED_BREP_SHAPE_REPRESENTATION('',(#281),#8360);
#350=STYLED_ITEM('',(#8725),#281);
#429=FACE_BOUND('',#1025,.T.);
#536=PLANE('',#4800);
#537=PLANE('',#4808);
#538=PLANE('',#4816);
#539=PLANE('',#4817);
#540=PLANE('',#4818);
#541=PLANE('',#4819);
#542=PLANE('',#4820);
#543=PLANE('',#4821);
#544=PLANE('',#4822);
#545=PLANE('',#4823);
#546=PLANE('',#4824);
#730=FACE_OUTER_BOUND('',#1020,.T.);
#731=FACE_OUTER_BOUND('',#1021,.T.);
#732=FACE_OUTER_BOUND('',#1022,.T.);
#733=FACE_OUTER_BOUND('',#1023,.T.);
#734=FACE_OUTER_BOUND('',#1024,.T.);
#735=FACE_OUTER_BOUND('',#1026,.T.);
#736=FACE_OUTER_BOUND('',#1027,.T.);
#737=FACE_OUTER_BOUND('',#1028,.T.);
#738=FACE_OUTER_BOUND('',#1029,.T.);
#739=FACE_OUTER_BOUND('',#1030,.T.);
#740=FACE_OUTER_BOUND('',#1031,.T.);
#741=FACE_OUTER_BOUND('',#1032,.T.);
#742=FACE_OUTER_BOUND('',#1033,.T.);
#743=FACE_OUTER_BOUND('',#1034,.T.);
#744=FACE_OUTER_BOUND('',#1035,.T.);
#745=FACE_OUTER_BOUND('',#1036,.T.);
#746=FACE_OUTER_BOUND('',#1037,.T.);
#1020=EDGE_LOOP('',(#3237));
#1021=EDGE_LOOP('',(#3238,#3239,#3240,#3241));
#1022=EDGE_LOOP('',(#3242,#3243,#3244,#3245));
#1023=EDGE_LOOP('',(#3246,#3247,#3248,#3249));
#1024=EDGE_LOOP('',(#3250));
#1025=EDGE_LOOP('',(#3251));
#1026=EDGE_LOOP('',(#3252,#3253,#3254,#3255));
#1027=EDGE_LOOP('',(#3256,#3257,#3258,#3259));
#1028=EDGE_LOOP('',(#3260,#3261,#3262,#3263));
#1029=EDGE_LOOP('',(#3264));
#1030=EDGE_LOOP('',(#3265,#3266,#3267,#3268));
#1031=EDGE_LOOP('',(#3269,#3270,#3271,#3272));
#1032=EDGE_LOOP('',(#3273,#3274,#3275,#3276));
#1033=EDGE_LOOP('',(#3277,#3278,#3279,#3280));
#1034=EDGE_LOOP('',(#3281,#3282,#3283,#3284));
#1035=EDGE_LOOP('',(#3285,#3286,#3287,#3288));
#1036=EDGE_LOOP('',(#3289,#3290,#3291,#3292,#3293,#3294));
#1037=EDGE_LOOP('',(#3295,#3296,#3297,#3298,#3299,#3300));
#1343=LINE('',#6802,#1670);
#1344=LINE('',#6806,#1671);
#1345=LINE('',#6810,#1672);
#1346=LINE('',#6817,#1673);
#1347=LINE('',#6821,#1674);
#1348=LINE('',#6825,#1675);
#1349=LINE('',#6830,#1676);
#1350=LINE('',#6832,#1677);
#1351=LINE('',#6834,#1678);
#1352=LINE('',#6835,#1679);
#1353=LINE('',#6838,#1680);
#1354=LINE('',#6840,#1681);
#1355=LINE('',#6841,#1682);
#1356=LINE('',#6844,#1683);
#1357=LINE('',#6846,#1684);
#1358=LINE('',#6847,#1685);
#1359=LINE('',#6850,#1686);
#1360=LINE('',#6852,#1687);
#1361=LINE('',#6853,#1688);
#1362=LINE('',#6856,#1689);
#1363=LINE('',#6858,#1690);
#1364=LINE('',#6859,#1691);
#1365=LINE('',#6861,#1692);
#1366=LINE('',#6862,#1693);
#1670=VECTOR('',#5538,0.475);
#1671=VECTOR('',#5543,0.5);
#1672=VECTOR('',#5548,0.485);
#1673=VECTOR('',#5557,0.31);
#1674=VECTOR('',#5562,0.3);
#1675=VECTOR('',#5567,0.27);
#1676=VECTOR('',#5572,1.);
#1677=VECTOR('',#5573,1.);
#1678=VECTOR('',#5574,1.);
#1679=VECTOR('',#5575,1.);
#1680=VECTOR('',#5578,1.);
#1681=VECTOR('',#5579,1.);
#1682=VECTOR('',#5580,1.);
#1683=VECTOR('',#5583,1.);
#1684=VECTOR('',#5584,1.);
#1685=VECTOR('',#5585,1.);
#1686=VECTOR('',#5588,1.);
#1687=VECTOR('',#5589,1.);
#1688=VECTOR('',#5590,1.);
#1689=VECTOR('',#5593,1.);
#1690=VECTOR('',#5594,1.);
#1691=VECTOR('',#5595,1.);
#1692=VECTOR('',#5598,1.);
#1693=VECTOR('',#5599,1.);
#1965=CIRCLE('',#4801,0.45);
#1966=CIRCLE('',#4803,0.5);
#1967=CIRCLE('',#4805,0.5);
#1968=CIRCLE('',#4807,0.47);
#1969=CIRCLE('',#4809,0.32);
#1970=CIRCLE('',#4811,0.2942);
#1971=CIRCLE('',#4813,0.2942);
#1972=CIRCLE('',#4815,0.24);
#2164=VERTEX_POINT('',#6797);
#2165=VERTEX_POINT('',#6800);
#2166=VERTEX_POINT('',#6804);
#2167=VERTEX_POINT('',#6808);
#2168=VERTEX_POINT('',#6812);
#2169=VERTEX_POINT('',#6815);
#2170=VERTEX_POINT('',#6819);
#2171=VERTEX_POINT('',#6823);
#2172=VERTEX_POINT('',#6828);
#2173=VERTEX_POINT('',#6829);
#2174=VERTEX_POINT('',#6831);
#2175=VERTEX_POINT('',#6833);
#2176=VERTEX_POINT('',#6837);
#2177=VERTEX_POINT('',#6839);
#2178=VERTEX_POINT('',#6843);
#2179=VERTEX_POINT('',#6845);
#2180=VERTEX_POINT('',#6849);
#2181=VERTEX_POINT('',#6851);
#2182=VERTEX_POINT('',#6855);
#2183=VERTEX_POINT('',#6857);
#2567=EDGE_CURVE('',#2164,#2164,#1965,.T.);
#2568=EDGE_CURVE('',#2165,#2165,#1966,.T.);
#2569=EDGE_CURVE('',#2165,#2164,#1343,.T.);
#2570=EDGE_CURVE('',#2166,#2166,#1967,.T.);
#2571=EDGE_CURVE('',#2166,#2165,#1344,.T.);
#2572=EDGE_CURVE('',#2167,#2167,#1968,.T.);
#2573=EDGE_CURVE('',#2167,#2166,#1345,.T.);
#2574=EDGE_CURVE('',#2168,#2168,#1969,.T.);
#2575=EDGE_CURVE('',#2169,#2169,#1970,.F.);
#2576=EDGE_CURVE('',#2169,#2168,#1346,.T.);
#2577=EDGE_CURVE('',#2170,#2170,#1971,.F.);
#2578=EDGE_CURVE('',#2170,#2169,#1347,.T.);
#2579=EDGE_CURVE('',#2171,#2171,#1972,.T.);
#2580=EDGE_CURVE('',#2171,#2170,#1348,.T.);
#2581=EDGE_CURVE('',#2172,#2173,#1349,.T.);
#2582=EDGE_CURVE('',#2173,#2174,#1350,.T.);
#2583=EDGE_CURVE('',#2174,#2175,#1351,.T.);
#2584=EDGE_CURVE('',#2172,#2175,#1352,.T.);
#2585=EDGE_CURVE('',#2173,#2176,#1353,.T.);
#2586=EDGE_CURVE('',#2176,#2177,#1354,.T.);
#2587=EDGE_CURVE('',#2177,#2174,#1355,.T.);
#2588=EDGE_CURVE('',#2176,#2178,#1356,.T.);
#2589=EDGE_CURVE('',#2178,#2179,#1357,.T.);
#2590=EDGE_CURVE('',#2179,#2177,#1358,.T.);
#2591=EDGE_CURVE('',#2178,#2180,#1359,.T.);
#2592=EDGE_CURVE('',#2180,#2181,#1360,.T.);
#2593=EDGE_CURVE('',#2181,#2179,#1361,.T.);
#2594=EDGE_CURVE('',#2180,#2182,#1362,.T.);
#2595=EDGE_CURVE('',#2182,#2183,#1363,.T.);
#2596=EDGE_CURVE('',#2183,#2181,#1364,.T.);
#2597=EDGE_CURVE('',#2182,#2172,#1365,.T.);
#2598=EDGE_CURVE('',#2175,#2183,#1366,.T.);
#3237=ORIENTED_EDGE('',*,*,#2567,.F.);
#3238=ORIENTED_EDGE('',*,*,#2568,.F.);
#3239=ORIENTED_EDGE('',*,*,#2569,.T.);
#3240=ORIENTED_EDGE('',*,*,#2567,.T.);
#3241=ORIENTED_EDGE('',*,*,#2569,.F.);
#3242=ORIENTED_EDGE('',*,*,#2570,.F.);
#3243=ORIENTED_EDGE('',*,*,#2571,.T.);
#3244=ORIENTED_EDGE('',*,*,#2568,.T.);
#3245=ORIENTED_EDGE('',*,*,#2571,.F.);
#3246=ORIENTED_EDGE('',*,*,#2572,.F.);
#3247=ORIENTED_EDGE('',*,*,#2573,.T.);
#3248=ORIENTED_EDGE('',*,*,#2570,.T.);
#3249=ORIENTED_EDGE('',*,*,#2573,.F.);
#3250=ORIENTED_EDGE('',*,*,#2572,.T.);
#3251=ORIENTED_EDGE('',*,*,#2574,.F.);
#3252=ORIENTED_EDGE('',*,*,#2575,.F.);
#3253=ORIENTED_EDGE('',*,*,#2576,.T.);
#3254=ORIENTED_EDGE('',*,*,#2574,.T.);
#3255=ORIENTED_EDGE('',*,*,#2576,.F.);
#3256=ORIENTED_EDGE('',*,*,#2577,.F.);
#3257=ORIENTED_EDGE('',*,*,#2578,.T.);
#3258=ORIENTED_EDGE('',*,*,#2575,.T.);
#3259=ORIENTED_EDGE('',*,*,#2578,.F.);
#3260=ORIENTED_EDGE('',*,*,#2579,.F.);
#3261=ORIENTED_EDGE('',*,*,#2580,.T.);
#3262=ORIENTED_EDGE('',*,*,#2577,.T.);
#3263=ORIENTED_EDGE('',*,*,#2580,.F.);
#3264=ORIENTED_EDGE('',*,*,#2579,.T.);
#3265=ORIENTED_EDGE('',*,*,#2581,.T.);
#3266=ORIENTED_EDGE('',*,*,#2582,.T.);
#3267=ORIENTED_EDGE('',*,*,#2583,.T.);
#3268=ORIENTED_EDGE('',*,*,#2584,.F.);
#3269=ORIENTED_EDGE('',*,*,#2585,.T.);
#3270=ORIENTED_EDGE('',*,*,#2586,.T.);
#3271=ORIENTED_EDGE('',*,*,#2587,.T.);
#3272=ORIENTED_EDGE('',*,*,#2582,.F.);
#3273=ORIENTED_EDGE('',*,*,#2588,.T.);
#3274=ORIENTED_EDGE('',*,*,#2589,.T.);
#3275=ORIENTED_EDGE('',*,*,#2590,.T.);
#3276=ORIENTED_EDGE('',*,*,#2586,.F.);
#3277=ORIENTED_EDGE('',*,*,#2591,.T.);
#3278=ORIENTED_EDGE('',*,*,#2592,.T.);
#3279=ORIENTED_EDGE('',*,*,#2593,.T.);
#3280=ORIENTED_EDGE('',*,*,#2589,.F.);
#3281=ORIENTED_EDGE('',*,*,#2594,.T.);
#3282=ORIENTED_EDGE('',*,*,#2595,.T.);
#3283=ORIENTED_EDGE('',*,*,#2596,.T.);
#3284=ORIENTED_EDGE('',*,*,#2592,.F.);
#3285=ORIENTED_EDGE('',*,*,#2597,.T.);
#3286=ORIENTED_EDGE('',*,*,#2584,.T.);
#3287=ORIENTED_EDGE('',*,*,#2598,.T.);
#3288=ORIENTED_EDGE('',*,*,#2595,.F.);
#3289=ORIENTED_EDGE('',*,*,#2597,.F.);
#3290=ORIENTED_EDGE('',*,*,#2594,.F.);
#3291=ORIENTED_EDGE('',*,*,#2591,.F.);
#3292=ORIENTED_EDGE('',*,*,#2588,.F.);
#3293=ORIENTED_EDGE('',*,*,#2585,.F.);
#3294=ORIENTED_EDGE('',*,*,#2581,.F.);
#3295=ORIENTED_EDGE('',*,*,#2598,.F.);
#3296=ORIENTED_EDGE('',*,*,#2583,.F.);
#3297=ORIENTED_EDGE('',*,*,#2587,.F.);
#3298=ORIENTED_EDGE('',*,*,#2590,.F.);
#3299=ORIENTED_EDGE('',*,*,#2593,.F.);
#3300=ORIENTED_EDGE('',*,*,#2596,.F.);
#4029=CYLINDRICAL_SURFACE('',#4804,0.5);
#4030=CYLINDRICAL_SURFACE('',#4812,0.2942);
#4148=ADVANCED_FACE('',(#730),#536,.T.);
#4149=ADVANCED_FACE('',(#731),#268,.T.);
#4150=ADVANCED_FACE('',(#732),#4029,.T.);
#4151=ADVANCED_FACE('',(#733),#269,.T.);
#4152=ADVANCED_FACE('',(#734,#429),#537,.T.);
#4153=ADVANCED_FACE('',(#735),#270,.T.);
#4154=ADVANCED_FACE('',(#736),#4030,.T.);
#4155=ADVANCED_FACE('',(#737),#271,.T.);
#4156=ADVANCED_FACE('',(#738),#538,.T.);
#4157=ADVANCED_FACE('',(#739),#539,.F.);
#4158=ADVANCED_FACE('',(#740),#540,.F.);
#4159=ADVANCED_FACE('',(#741),#541,.F.);
#4160=ADVANCED_FACE('',(#742),#542,.F.);
#4161=ADVANCED_FACE('',(#743),#543,.F.);
#4162=ADVANCED_FACE('',(#744),#544,.F.);
#4163=ADVANCED_FACE('',(#745),#545,.F.);
#4164=ADVANCED_FACE('',(#746),#546,.F.);
#4336=CLOSED_SHELL('',(#4148,#4149,#4150,#4151,#4152,#4153,#4154,#4155,
#4156));
#4337=CLOSED_SHELL('',(#4157,#4158,#4159,#4160,#4161,#4162,#4163,#4164));
#4799=AXIS2_PLACEMENT_3D('',#6795,#5528,#5529);
#4800=AXIS2_PLACEMENT_3D('',#6796,#5530,#5531);
#4801=AXIS2_PLACEMENT_3D('',#6798,#5532,#5533);
#4802=AXIS2_PLACEMENT_3D('',#6799,#5534,#5535);
#4803=AXIS2_PLACEMENT_3D('',#6801,#5536,#5537);
#4804=AXIS2_PLACEMENT_3D('',#6803,#5539,#5540);
#4805=AXIS2_PLACEMENT_3D('',#6805,#5541,#5542);
#4806=AXIS2_PLACEMENT_3D('',#6807,#5544,#5545);
#4807=AXIS2_PLACEMENT_3D('',#6809,#5546,#5547);
#4808=AXIS2_PLACEMENT_3D('',#6811,#5549,#5550);
#4809=AXIS2_PLACEMENT_3D('',#6813,#5551,#5552);
#4810=AXIS2_PLACEMENT_3D('',#6814,#5553,#5554);
#4811=AXIS2_PLACEMENT_3D('',#6816,#5555,#5556);
#4812=AXIS2_PLACEMENT_3D('',#6818,#5558,#5559);
#4813=AXIS2_PLACEMENT_3D('',#6820,#5560,#5561);
#4814=AXIS2_PLACEMENT_3D('',#6822,#5563,#5564);
#4815=AXIS2_PLACEMENT_3D('',#6824,#5565,#5566);
#4816=AXIS2_PLACEMENT_3D('',#6826,#5568,#5569);
#4817=AXIS2_PLACEMENT_3D('',#6827,#5570,#5571);
#4818=AXIS2_PLACEMENT_3D('',#6836,#5576,#5577);
#4819=AXIS2_PLACEMENT_3D('',#6842,#5581,#5582);
#4820=AXIS2_PLACEMENT_3D('',#6848,#5586,#5587);
#4821=AXIS2_PLACEMENT_3D('',#6854,#5591,#5592);
#4822=AXIS2_PLACEMENT_3D('',#6860,#5596,#5597);
#4823=AXIS2_PLACEMENT_3D('',#6863,#5600,#5601);
#4824=AXIS2_PLACEMENT_3D('',#6864,#5602,#5603);
#5528=DIRECTION('axis',(0.,0.,1.));
#5529=DIRECTION('refdir',(1.,0.,0.));
#5530=DIRECTION('center_axis',(0.,1.,0.));
#5531=DIRECTION('ref_axis',(0.,0.,1.));
#5532=DIRECTION('center_axis',(0.,-1.,0.));
#5533=DIRECTION('ref_axis',(1.,0.,0.));
#5534=DIRECTION('center_axis',(0.,-1.,0.));
#5535=DIRECTION('ref_axis',(1.,0.,0.));
#5536=DIRECTION('center_axis',(0.,-1.,0.));
#5537=DIRECTION('ref_axis',(1.,0.,0.));
#5538=DIRECTION('',(0.707106781186548,0.707106781186547,8.65956056235494E-17));
#5539=DIRECTION('center_axis',(0.,-1.,0.));
#5540=DIRECTION('ref_axis',(1.,0.,0.));
#5541=DIRECTION('center_axis',(0.,-1.,0.));
#5542=DIRECTION('ref_axis',(1.,0.,0.));
#5543=DIRECTION('',(0.,1.,0.));
#5544=DIRECTION('center_axis',(0.,1.,0.));
#5545=DIRECTION('ref_axis',(1.,0.,0.));
#5546=DIRECTION('center_axis',(0.,-1.,0.));
#5547=DIRECTION('ref_axis',(1.,0.,0.));
#5548=DIRECTION('',(-0.707106781186547,0.707106781186548,-8.65956056235493E-17));
#5549=DIRECTION('center_axis',(0.,-1.,0.));
#5550=DIRECTION('ref_axis',(0.,0.,-1.));
#5551=DIRECTION('center_axis',(0.,-1.,0.));
#5552=DIRECTION('ref_axis',(1.,0.,0.));
#5553=DIRECTION('center_axis',(0.,1.,0.));
#5554=DIRECTION('ref_axis',(1.,0.,0.));
#5555=DIRECTION('center_axis',(0.,1.,0.));
#5556=DIRECTION('ref_axis',(1.,0.,0.));
#5557=DIRECTION('',(-0.447213595499958,0.894427190999916,-5.47678698264203E-17));
#5558=DIRECTION('center_axis',(0.,-1.,0.));
#5559=DIRECTION('ref_axis',(1.,0.,0.));
#5560=DIRECTION('center_axis',(0.,1.,0.));
#5561=DIRECTION('ref_axis',(1.,0.,0.));
#5562=DIRECTION('',(0.,1.,0.));
#5563=DIRECTION('center_axis',(0.,1.,0.));
#5564=DIRECTION('ref_axis',(1.,0.,0.));
#5565=DIRECTION('center_axis',(0.,-1.,0.));
#5566=DIRECTION('ref_axis',(1.,0.,0.));
#5567=DIRECTION('',(-0.707106781186547,0.707106781186548,-8.65956056235493E-17));
#5568=DIRECTION('center_axis',(0.,-1.,0.));
#5569=DIRECTION('ref_axis',(0.,0.,-1.));
#5570=DIRECTION('center_axis',(0.866025403784439,0.,-0.5));
#5571=DIRECTION('ref_axis',(0.5,0.,0.866025403784439));
#5572=DIRECTION('',(-0.5,0.,-0.866025403784439));
#5573=DIRECTION('',(0.,-1.,0.));
#5574=DIRECTION('',(0.5,0.,0.866025403784439));
#5575=DIRECTION('',(0.,-1.,0.));
#5576=DIRECTION('center_axis',(1.92296268638356E-16,0.,-1.));
#5577=DIRECTION('ref_axis',(1.,0.,1.92296268638356E-16));
#5578=DIRECTION('',(-1.,0.,-1.92296268638356E-16));
#5579=DIRECTION('',(0.,-1.,0.));
#5580=DIRECTION('',(1.,0.,1.92296268638356E-16));
#5581=DIRECTION('center_axis',(-0.866025403784439,0.,-0.5));
#5582=DIRECTION('ref_axis',(0.5,0.,-0.866025403784439));
#5583=DIRECTION('',(-0.5,0.,0.866025403784438));
#5584=DIRECTION('',(0.,-1.,0.));
#5585=DIRECTION('',(0.5,0.,-0.866025403784438));
#5586=DIRECTION('center_axis',(-0.866025403784439,0.,0.5));
#5587=DIRECTION('ref_axis',(-0.5,0.,-0.866025403784439));
#5588=DIRECTION('',(0.5,0.,0.866025403784439));
#5589=DIRECTION('',(0.,-1.,0.));
#5590=DIRECTION('',(-0.5,0.,-0.866025403784439));
#5591=DIRECTION('center_axis',(-1.92296268638356E-16,0.,1.));
#5592=DIRECTION('ref_axis',(-1.,0.,-1.92296268638356E-16));
#5593=DIRECTION('',(1.,0.,1.92296268638356E-16));
#5594=DIRECTION('',(0.,-1.,0.));
#5595=DIRECTION('',(-1.,0.,-1.92296268638356E-16));
#5596=DIRECTION('center_axis',(0.866025403784439,0.,0.5));
#5597=DIRECTION('ref_axis',(-0.5,0.,0.866025403784439));
#5598=DIRECTION('',(0.5,0.,-0.866025403784439));
#5599=DIRECTION('',(-0.5,0.,0.866025403784439));
#5600=DIRECTION('center_axis',(0.,1.,0.));
#5601=DIRECTION('ref_axis',(1.,0.,0.));
#5602=DIRECTION('center_axis',(0.,-1.,0.));
#5603=DIRECTION('ref_axis',(0.,0.,-1.));
#6795=CARTESIAN_POINT('',(0.,0.,0.));
#6796=CARTESIAN_POINT('Origin',(0.45,0.6,0.));
#6797=CARTESIAN_POINT('',(-0.45,0.6,-5.51091059616309E-17));
#6798=CARTESIAN_POINT('Origin',(0.,0.6,0.));
#6799=CARTESIAN_POINT('Origin',(0.,0.575,0.));
#6800=CARTESIAN_POINT('',(-0.5,0.55,-6.12323399573677E-17));
#6801=CARTESIAN_POINT('Origin',(0.,0.55,0.));
#6802=CARTESIAN_POINT('',(-0.475,0.575,-5.81707229594993E-17));
#6803=CARTESIAN_POINT('Origin',(0.,0.29,0.));
#6804=CARTESIAN_POINT('',(-0.5,0.0299999999999998,-6.12323399573677E-17));
#6805=CARTESIAN_POINT('Origin',(0.,0.0299999999999998,0.));
#6806=CARTESIAN_POINT('',(-0.5,0.29,-6.12323399573677E-17));
#6807=CARTESIAN_POINT('Origin',(0.,0.0150000000000001,0.));
#6808=CARTESIAN_POINT('',(-0.47,7.11236625150491E-17,-5.75583995599256E-17));
#6809=CARTESIAN_POINT('Origin',(0.,0.,0.));
#6810=CARTESIAN_POINT('',(-0.485,0.0150000000000001,-5.93953697586466E-17));
#6811=CARTESIAN_POINT('Origin',(0.32,0.,0.));
#6812=CARTESIAN_POINT('',(-0.32,-6.93889390390723E-18,-3.91886975727153E-17));
#6813=CARTESIAN_POINT('Origin',(0.,0.,0.));
#6814=CARTESIAN_POINT('Origin',(0.,-0.02,0.));
#6815=CARTESIAN_POINT('',(-0.2942,-0.0515999999999999,3.60291088309151E-17));
#6816=CARTESIAN_POINT('Origin',(0.,-0.0515999999999999,0.));
#6817=CARTESIAN_POINT('',(-0.31,-0.02,-3.7964050773568E-17));
#6818=CARTESIAN_POINT('Origin',(0.,-1.24,0.));
#6819=CARTESIAN_POINT('',(-0.2942,-2.4458,3.60291088309151E-17));
#6820=CARTESIAN_POINT('Origin',(0.,-2.4458,0.));
#6821=CARTESIAN_POINT('',(-0.2942,-1.24,-3.60291088309151E-17));
#6822=CARTESIAN_POINT('Origin',(0.,-2.47,0.));
#6823=CARTESIAN_POINT('',(-0.24,-2.5,-2.93915231795365E-17));
#6824=CARTESIAN_POINT('Origin',(0.,-2.5,0.));
#6825=CARTESIAN_POINT('',(-0.27,-2.47,-3.30654635769785E-17));
#6826=CARTESIAN_POINT('Origin',(0.,-2.5,0.));
#6827=CARTESIAN_POINT('Origin',(0.144337567297406,-0.6,-0.25));
#6828=CARTESIAN_POINT('',(0.288675134594813,-0.6,0.));
#6829=CARTESIAN_POINT('',(0.144337567297406,-0.6,-0.25));
#6830=CARTESIAN_POINT('',(0.288675134594813,-0.6,0.));
#6831=CARTESIAN_POINT('',(0.144337567297406,-0.96,-0.25));
#6832=CARTESIAN_POINT('',(0.144337567297406,-0.6,-0.25));
#6833=CARTESIAN_POINT('',(0.288675134594813,-0.96,0.));
#6834=CARTESIAN_POINT('',(0.288675134594813,-0.96,0.));
#6835=CARTESIAN_POINT('',(0.288675134594813,-0.6,0.));
#6836=CARTESIAN_POINT('Origin',(-0.144337567297406,-0.6,-0.25));
#6837=CARTESIAN_POINT('',(-0.144337567297406,-0.6,-0.25));
#6838=CARTESIAN_POINT('',(0.144337567297406,-0.6,-0.25));
#6839=CARTESIAN_POINT('',(-0.144337567297406,-0.96,-0.25));
#6840=CARTESIAN_POINT('',(-0.144337567297406,-0.6,-0.25));
#6841=CARTESIAN_POINT('',(0.144337567297406,-0.96,-0.25));
#6842=CARTESIAN_POINT('Origin',(-0.288675134594813,-0.6,-8.32667268468867E-17));
#6843=CARTESIAN_POINT('',(-0.288675134594813,-0.6,-3.53525079574969E-17));
#6844=CARTESIAN_POINT('',(-0.144337567297406,-0.6,-0.25));
#6845=CARTESIAN_POINT('',(-0.288675134594813,-0.96,-5.55111512312578E-17));
#6846=CARTESIAN_POINT('',(-0.288675134594813,-0.6,-3.53525079574969E-17));
#6847=CARTESIAN_POINT('',(-0.144337567297406,-0.96,-0.25));
#6848=CARTESIAN_POINT('Origin',(-0.144337567297407,-0.6,0.25));
#6849=CARTESIAN_POINT('',(-0.144337567297407,-0.6,0.25));
#6850=CARTESIAN_POINT('',(-0.288675134594813,-0.6,-3.53525079574969E-17));
#6851=CARTESIAN_POINT('',(-0.144337567297407,-0.96,0.25));
#6852=CARTESIAN_POINT('',(-0.144337567297407,-0.6,0.25));
#6853=CARTESIAN_POINT('',(-0.288675134594813,-0.96,-3.53525079574969E-17));
#6854=CARTESIAN_POINT('Origin',(0.144337567297406,-0.6,0.25));
#6855=CARTESIAN_POINT('',(0.144337567297406,-0.6,0.25));
#6856=CARTESIAN_POINT('',(-0.144337567297407,-0.6,0.25));
#6857=CARTESIAN_POINT('',(0.144337567297406,-0.96,0.25));
#6858=CARTESIAN_POINT('',(0.144337567297406,-0.6,0.25));
#6859=CARTESIAN_POINT('',(-0.144337567297407,-0.96,0.25));
#6860=CARTESIAN_POINT('Origin',(0.288675134594813,-0.6,0.));
#6861=CARTESIAN_POINT('',(0.144337567297406,-0.6,0.25));
#6862=CARTESIAN_POINT('',(0.144337567297406,-0.96,0.25));
#6863=CARTESIAN_POINT('Origin',(0.,-0.6,0.));
#6864=CARTESIAN_POINT('Origin',(0.,-0.96,0.));
#8328=UNCERTAINTY_MEASURE_WITH_UNIT(LENGTH_MEASURE(0.001),#8378,
'DISTANCE_ACCURACY_VALUE',
'Maximum model space distance between geometric entities at asserted c
onnectivities');
#8345=UNCERTAINTY_MEASURE_WITH_UNIT(LENGTH_MEASURE(0.001),#8378,
'DISTANCE_ACCURACY_VALUE',
'Maximum model space distance between geometric entities at asserted c
onnectivities');
#8360=(
GEOMETRIC_REPRESENTATION_CONTEXT(3)
GLOBAL_UNCERTAINTY_ASSIGNED_CONTEXT((#8328))
GLOBAL_UNIT_ASSIGNED_CONTEXT((#8378,#8380,#8381))
REPRESENTATION_CONTEXT('','3D')
);
#8377=(
GEOMETRIC_REPRESENTATION_CONTEXT(3)
GLOBAL_UNCERTAINTY_ASSIGNED_CONTEXT((#8345))
GLOBAL_UNIT_ASSIGNED_CONTEXT((#8378,#8380,#8381))
REPRESENTATION_CONTEXT('','3D')
);
#8378=(
LENGTH_UNIT()
NAMED_UNIT(*)
SI_UNIT(.CENTI.,.METRE.)
);
#8380=(
NAMED_UNIT(*)
PLANE_ANGLE_UNIT()
SI_UNIT($,.RADIAN.)
);
#8381=(
NAMED_UNIT(*)
SI_UNIT($,.STERADIAN.)
SOLID_ANGLE_UNIT()
);
#8396=SHAPE_DEFINITION_REPRESENTATION(#8427,#8511);
#8427=PRODUCT_DEFINITION_SHAPE('',$,#8543);
#8511=SHAPE_REPRESENTATION('',(#4799),#8360);
#8528=PRODUCT_DEFINITION_CONTEXT('part definition',#8623,'design');
#8543=PRODUCT_DEFINITION('Cap Screw - M6x25','Cap Screw - M6x25',#8574,
#8528);
#8574=PRODUCT_DEFINITION_FORMATION('',$,#8639);
#8623=APPLICATION_CONTEXT(
'Core Data for Automotive Mechanical Design Process');
#8624=PRODUCT_CONTEXT('part definition',#8623,'mechanical');
#8639=PRODUCT('Cap Screw - M6x25','Cap Screw - M6x25',
'Cap Screw - M6x25',(#8624));
#8719=COLOUR_RGB('Black',0.12,0.14,0.17);
#8720=FILL_AREA_STYLE_COLOUR('',#8719);
#8721=FILL_AREA_STYLE('',(#8720));
#8722=SURFACE_STYLE_FILL_AREA(#8721);
#8723=SURFACE_SIDE_STYLE('',(#8722));
#8724=SURFACE_STYLE_USAGE(.BOTH.,#8723);
#8725=PRESENTATION_STYLE_ASSIGNMENT((#8724));
ENDSEC;
END-ISO-10303-21;
